ISO-10303-21;
HEADER;
/* Generated by software containing ST-Developer
 * from STEP Tools, Inc. (www.steptools.com) 
 */

FILE_DESCRIPTION(
/* description */ ('Shaft runout checking stand'),
/* implementation_level */ '2;1');

FILE_NAME(
/* name */ 'Captive slot nut.step',
/* time_stamp */ '2026-11-02T21:12:33-08:00',
/* author */ (''),
/* organization */ (''),
/* preprocessor_version */ 'ST-DEVELOPER v20.2',
/* originating_system */ 'Autodesk Translation Framework v15.17.0.0',
/* authorisation */ '');

FILE_SCHEMA (('AUTOMOTIVE_DESIGN { 1 0 10303 214 3 1 1 }'));
ENDSEC;

DATA;
#10=MECHANICAL_DESIGN_GEOMETRIC_PRESENTATION_REPRESENTATION('',(#465),#11748);
#375=ELLIPSE('',#6840,0.299389011154384,0.2117);
#376=ELLIPSE('',#6844,0.299389011154384,0.2117);
#379=SHAPE_REPRESENTATION_RELATIONSHIP('SRR','None',#11928,#422);
#422=ADVANCED_BREP_SHAPE_REPRESENTATION('',(#516),#11704);
#465=STYLED_ITEM('',(#12169),#516);
#516=MANIFOLD_SOLID_BREP('Body1',#6208);
#588=FACE_BOUND('',#1500,.T.);
#699=CIRCLE('',#6833,0.2117);
#700=CIRCLE('',#6842,0.2117);
#701=CIRCLE('',#6843,0.2117);
#702=CIRCLE('',#6845,0.2117);
#951=CYLINDRICAL_SURFACE('',#6841,0.2117);
#1103=FACE_OUTER_BOUND('',#1497,.T.);
#1104=FACE_OUTER_BOUND('',#1498,.T.);
#1105=FACE_OUTER_BOUND('',#1499,.T.);
#1106=FACE_OUTER_BOUND('',#1501,.T.);
#1107=FACE_OUTER_BOUND('',#1502,.T.);
#1108=FACE_OUTER_BOUND('',#1503,.T.);
#1109=FACE_OUTER_BOUND('',#1504,.T.);
#1110=FACE_OUTER_BOUND('',#1505,.T.);
#1111=FACE_OUTER_BOUND('',#1506,.T.);
#1112=FACE_OUTER_BOUND('',#1507,.T.);
#1113=FACE_OUTER_BOUND('',#1508,.T.);
#1114=FACE_OUTER_BOUND('',#1509,.T.);
#1115=FACE_OUTER_BOUND('',#1510,.T.);
#1116=FACE_OUTER_BOUND('',#1511,.T.);
#1497=EDGE_LOOP('',(#4454,#4455,#4456,#4457));
#1498=EDGE_LOOP('',(#4458,#4459,#4460,#4461));
#1499=EDGE_LOOP('',(#4462,#4463,#4464,#4465));
#1500=EDGE_LOOP('',(#4466));
#1501=EDGE_LOOP('',(#4467,#4468,#4469,#4470,#4471,#4472,#4473,#4474,#4475,
#4476));
#1502=EDGE_LOOP('',(#4477,#4478,#4479,#4480));
#1503=EDGE_LOOP('',(#4481,#4482,#4483,#4484));
#1504=EDGE_LOOP('',(#4485,#4486,#4487,#4488,#4489,#4490,#4491,#4492,#4493,
#4494));
#1505=EDGE_LOOP('',(#4495,#4496,#4497,#4498));
#1506=EDGE_LOOP('',(#4499,#4500,#4501,#4502,#4503,#4504));
#1507=EDGE_LOOP('',(#4505,#4506,#4507,#4508,#4509,#4510,#4511,#4512));
#1508=EDGE_LOOP('',(#4513,#4514,#4515,#4516,#4517));
#1509=EDGE_LOOP('',(#4518,#4519,#4520,#4521));
#1510=EDGE_LOOP('',(#4522,#4523,#4524,#4525,#4526,#4527));
#1511=EDGE_LOOP('',(#4528,#4529,#4530,#4531));
#2042=LINE('',#9853,#2509);
#2043=LINE('',#9855,#2510);
#2044=LINE('',#9857,#2511);
#2045=LINE('',#9858,#2512);
#2046=LINE('',#9861,#2513);
#2047=LINE('',#9863,#2514);
#2048=LINE('',#9864,#2515);
#2049=LINE('',#9867,#2516);
#2050=LINE('',#9869,#2517);
#2051=LINE('',#9870,#2518);
#2052=LINE('',#9875,#2519);
#2053=LINE('',#9877,#2520);
#2054=LINE('',#9879,#2521);
#2055=LINE('',#9881,#2522);
#2056=LINE('',#9883,#2523);
#2057=LINE('',#9885,#2524);
#2058=LINE('',#9886,#2525);
#2059=LINE('',#9889,#2526);
#2060=LINE('',#9890,#2527);
#2061=LINE('',#9893,#2528);
#2062=LINE('',#9894,#2529);
#2063=LINE('',#9897,#2530);
#2064=LINE('',#9899,#2531);
#2065=LINE('',#9901,#2532);
#2066=LINE('',#9903,#2533);
#2067=LINE('',#9904,#2534);
#2068=LINE('',#9906,#2535);
#2069=LINE('',#9909,#2536);
#2070=LINE('',#9912,#2537);
#2071=LINE('',#9916,#2538);
#2072=LINE('',#9923,#2539);
#2073=LINE('',#9925,#2540);
#2074=LINE('',#9927,#2541);
#2509=VECTOR('',#7843,1.);
#2510=VECTOR('',#7844,1.);
#2511=VECTOR('',#7845,1.);
#2512=VECTOR('',#7846,1.);
#2513=VECTOR('',#7849,1.);
#2514=VECTOR('',#7850,1.);
#2515=VECTOR('',#7851,1.);
#2516=VECTOR('',#7854,1.);
#2517=VECTOR('',#7855,1.);
#2518=VECTOR('',#7856,1.);
#2519=VECTOR('',#7861,1.);
#2520=VECTOR('',#7862,1.);
#2521=VECTOR('',#7863,1.);
#2522=VECTOR('',#7864,1.);
#2523=VECTOR('',#7865,1.);
#2524=VECTOR('',#7866,1.);
#2525=VECTOR('',#7867,1.);
#2526=VECTOR('',#7870,1.);
#2527=VECTOR('',#7871,1.);
#2528=VECTOR('',#7874,1.);
#2529=VECTOR('',#7875,1.);
#2530=VECTOR('',#7878,1.);
#2531=VECTOR('',#7879,1.);
#2532=VECTOR('',#7880,1.);
#2533=VECTOR('',#7881,1.);
#2534=VECTOR('',#7882,1.);
#2535=VECTOR('',#7885,1.);
#2536=VECTOR('',#7888,1.);
#2537=VECTOR('',#7891,1.);
#2538=VECTOR('',#7896,0.21);
#2539=VECTOR('',#7905,1.);
#2540=VECTOR('',#7908,1.);
#2541=VECTOR('',#7911,1.);
#2941=VERTEX_POINT('',#9851);
#2942=VERTEX_POINT('',#9852);
#2943=VERTEX_POINT('',#9854);
#2944=VERTEX_POINT('',#9856);
#2945=VERTEX_POINT('',#9860);
#2946=VERTEX_POINT('',#9862);
#2947=VERTEX_POINT('',#9866);
#2948=VERTEX_POINT('',#9868);
#2949=VERTEX_POINT('',#9871);
#2950=VERTEX_POINT('',#9874);
#2951=VERTEX_POINT('',#9876);
#2952=VERTEX_POINT('',#9878);
#2953=VERTEX_POINT('',#9880);
#2954=VERTEX_POINT('',#9882);
#2955=VERTEX_POINT('',#9884);
#2956=VERTEX_POINT('',#9888);
#2957=VERTEX_POINT('',#9892);
#2958=VERTEX_POINT('',#9896);
#2959=VERTEX_POINT('',#9898);
#2960=VERTEX_POINT('',#9900);
#2961=VERTEX_POINT('',#9902);
#2962=VERTEX_POINT('',#9908);
#2963=VERTEX_POINT('',#9910);
#2964=VERTEX_POINT('',#9914);
#2965=VERTEX_POINT('',#9917);
#2966=VERTEX_POINT('',#9919);
#3513=EDGE_CURVE('',#2941,#2942,#2042,.T.);
#3514=EDGE_CURVE('',#2943,#2941,#2043,.T.);
#3515=EDGE_CURVE('',#2944,#2943,#2044,.T.);
#3516=EDGE_CURVE('',#2942,#2944,#2045,.T.);
#3517=EDGE_CURVE('',#2943,#2945,#2046,.T.);
#3518=EDGE_CURVE('',#2946,#2945,#2047,.T.);
#3519=EDGE_CURVE('',#2944,#2946,#2048,.T.);
#3520=EDGE_CURVE('',#2945,#2947,#2049,.T.);
#3521=EDGE_CURVE('',#2947,#2948,#2050,.T.);
#3522=EDGE_CURVE('',#2948,#2946,#2051,.T.);
#3523=EDGE_CURVE('',#2949,#2949,#699,.T.);
#3524=EDGE_CURVE('',#2950,#2941,#2052,.T.);
#3525=EDGE_CURVE('',#2951,#2950,#2053,.T.);
#3526=EDGE_CURVE('',#2951,#2952,#2054,.T.);
#3527=EDGE_CURVE('',#2953,#2952,#2055,.T.);
#3528=EDGE_CURVE('',#2953,#2954,#2056,.T.);
#3529=EDGE_CURVE('',#2954,#2955,#2057,.T.);
#3530=EDGE_CURVE('',#2955,#2947,#2058,.T.);
#3531=EDGE_CURVE('',#2955,#2956,#2059,.T.);
#3532=EDGE_CURVE('',#2956,#2948,#2060,.T.);
#3533=EDGE_CURVE('',#2957,#2954,#2061,.T.);
#3534=EDGE_CURVE('',#2956,#2957,#2062,.T.);
#3535=EDGE_CURVE('',#2958,#2957,#2063,.T.);
#3536=EDGE_CURVE('',#2959,#2958,#2064,.T.);
#3537=EDGE_CURVE('',#2959,#2960,#2065,.T.);
#3538=EDGE_CURVE('',#2961,#2960,#2066,.T.);
#3539=EDGE_CURVE('',#2961,#2942,#2067,.T.);
#3540=EDGE_CURVE('',#2958,#2953,#2068,.T.);
#3541=EDGE_CURVE('',#2952,#2962,#2069,.T.);
#3542=EDGE_CURVE('',#2962,#2963,#375,.T.);
#3543=EDGE_CURVE('',#2963,#2959,#2070,.T.);
#3544=EDGE_CURVE('',#2964,#2962,#700,.F.);
#3545=EDGE_CURVE('',#2964,#2949,#2071,.T.);
#3546=EDGE_CURVE('',#2965,#2964,#701,.F.);
#3547=EDGE_CURVE('',#2966,#2965,#376,.T.);
#3548=EDGE_CURVE('',#2963,#2966,#702,.F.);
#3549=EDGE_CURVE('',#2965,#2951,#2072,.T.);
#3550=EDGE_CURVE('',#2960,#2966,#2073,.T.);
#3551=EDGE_CURVE('',#2950,#2961,#2074,.T.);
#4454=ORIENTED_EDGE('',*,*,#3513,.F.);
#4455=ORIENTED_EDGE('',*,*,#3514,.F.);
#4456=ORIENTED_EDGE('',*,*,#3515,.F.);
#4457=ORIENTED_EDGE('',*,*,#3516,.F.);
#4458=ORIENTED_EDGE('',*,*,#3515,.T.);
#4459=ORIENTED_EDGE('',*,*,#3517,.T.);
#4460=ORIENTED_EDGE('',*,*,#3518,.F.);
#4461=ORIENTED_EDGE('',*,*,#3519,.F.);
#4462=ORIENTED_EDGE('',*,*,#3520,.T.);
#4463=ORIENTED_EDGE('',*,*,#3521,.T.);
#4464=ORIENTED_EDGE('',*,*,#3522,.T.);
#4465=ORIENTED_EDGE('',*,*,#3518,.T.);
#4466=ORIENTED_EDGE('',*,*,#3523,.T.);
#4467=ORIENTED_EDGE('',*,*,#3520,.F.);
#4468=ORIENTED_EDGE('',*,*,#3517,.F.);
#4469=ORIENTED_EDGE('',*,*,#3514,.T.);
#4470=ORIENTED_EDGE('',*,*,#3524,.F.);
#4471=ORIENTED_EDGE('',*,*,#3525,.F.);
#4472=ORIENTED_EDGE('',*,*,#3526,.T.);
#4473=ORIENTED_EDGE('',*,*,#3527,.F.);
#4474=ORIENTED_EDGE('',*,*,#3528,.T.);
#4475=ORIENTED_EDGE('',*,*,#3529,.T.);
#4476=ORIENTED_EDGE('',*,*,#3530,.T.);
#4477=ORIENTED_EDGE('',*,*,#3531,.T.);
#4478=ORIENTED_EDGE('',*,*,#3532,.T.);
#4479=ORIENTED_EDGE('',*,*,#3521,.F.);
#4480=ORIENTED_EDGE('',*,*,#3530,.F.);
#4481=ORIENTED_EDGE('',*,*,#3533,.F.);
#4482=ORIENTED_EDGE('',*,*,#3534,.F.);
#4483=ORIENTED_EDGE('',*,*,#3531,.F.);
#4484=ORIENTED_EDGE('',*,*,#3529,.F.);
#4485=ORIENTED_EDGE('',*,*,#3522,.F.);
#4486=ORIENTED_EDGE('',*,*,#3532,.F.);
#4487=ORIENTED_EDGE('',*,*,#3534,.T.);
#4488=ORIENTED_EDGE('',*,*,#3535,.F.);
#4489=ORIENTED_EDGE('',*,*,#3536,.F.);
#4490=ORIENTED_EDGE('',*,*,#3537,.T.);
#4491=ORIENTED_EDGE('',*,*,#3538,.F.);
#4492=ORIENTED_EDGE('',*,*,#3539,.T.);
#4493=ORIENTED_EDGE('',*,*,#3516,.T.);
#4494=ORIENTED_EDGE('',*,*,#3519,.T.);
#4495=ORIENTED_EDGE('',*,*,#3533,.T.);
#4496=ORIENTED_EDGE('',*,*,#3528,.F.);
#4497=ORIENTED_EDGE('',*,*,#3540,.F.);
#4498=ORIENTED_EDGE('',*,*,#3535,.T.);
#4499=ORIENTED_EDGE('',*,*,#3536,.T.);
#4500=ORIENTED_EDGE('',*,*,#3540,.T.);
#4501=ORIENTED_EDGE('',*,*,#3527,.T.);
#4502=ORIENTED_EDGE('',*,*,#3541,.T.);
#4503=ORIENTED_EDGE('',*,*,#3542,.T.);
#4504=ORIENTED_EDGE('',*,*,#3543,.T.);
#4505=ORIENTED_EDGE('',*,*,#3542,.F.);
#4506=ORIENTED_EDGE('',*,*,#3544,.F.);
#4507=ORIENTED_EDGE('',*,*,#3545,.T.);
#4508=ORIENTED_EDGE('',*,*,#3523,.F.);
#4509=ORIENTED_EDGE('',*,*,#3545,.F.);
#4510=ORIENTED_EDGE('',*,*,#3546,.F.);
#4511=ORIENTED_EDGE('',*,*,#3547,.F.);
#4512=ORIENTED_EDGE('',*,*,#3548,.F.);
#4513=ORIENTED_EDGE('',*,*,#3541,.F.);
#4514=ORIENTED_EDGE('',*,*,#3526,.F.);
#4515=ORIENTED_EDGE('',*,*,#3549,.F.);
#4516=ORIENTED_EDGE('',*,*,#3546,.T.);
#4517=ORIENTED_EDGE('',*,*,#3544,.T.);
#4518=ORIENTED_EDGE('',*,*,#3543,.F.);
#4519=ORIENTED_EDGE('',*,*,#3548,.T.);
#4520=ORIENTED_EDGE('',*,*,#3550,.F.);
#4521=ORIENTED_EDGE('',*,*,#3537,.F.);
#4522=ORIENTED_EDGE('',*,*,#3525,.T.);
#4523=ORIENTED_EDGE('',*,*,#3551,.T.);
#4524=ORIENTED_EDGE('',*,*,#3538,.T.);
#4525=ORIENTED_EDGE('',*,*,#3550,.T.);
#4526=ORIENTED_EDGE('',*,*,#3547,.T.);
#4527=ORIENTED_EDGE('',*,*,#3549,.T.);
#4528=ORIENTED_EDGE('',*,*,#3513,.T.);
#4529=ORIENTED_EDGE('',*,*,#3539,.F.);
#4530=ORIENTED_EDGE('',*,*,#3551,.F.);
#4531=ORIENTED_EDGE('',*,*,#3524,.T.);
#5656=PLANE('',#6830);
#5657=PLANE('',#6831);
#5658=PLANE('',#6832);
#5659=PLANE('',#6834);
#5660=PLANE('',#6835);
#5661=PLANE('',#6836);
#5662=PLANE('',#6837);
#5663=PLANE('',#6838);
#5664=PLANE('',#6839);
#5665=PLANE('',#6846);
#5666=PLANE('',#6847);
#5667=PLANE('',#6848);
#5668=PLANE('',#6849);
#5903=ADVANCED_FACE('',(#1103),#5656,.F.);
#5904=ADVANCED_FACE('',(#1104),#5657,.T.);
#5905=ADVANCED_FACE('',(#1105,#588),#5658,.T.);
#5906=ADVANCED_FACE('',(#1106),#5659,.T.);
#5907=ADVANCED_FACE('',(#1107),#5660,.T.);
#5908=ADVANCED_FACE('',(#1108),#5661,.F.);
#5909=ADVANCED_FACE('',(#1109),#5662,.T.);
#5910=ADVANCED_FACE('',(#1110),#5663,.T.);
#5911=ADVANCED_FACE('',(#1111),#5664,.T.);
#5912=ADVANCED_FACE('',(#1112),#951,.F.);
#5913=ADVANCED_FACE('',(#1113),#5665,.F.);
#5914=ADVANCED_FACE('',(#1114),#5666,.F.);
#5915=ADVANCED_FACE('',(#1115),#5667,.T.);
#5916=ADVANCED_FACE('',(#1116),#5668,.T.);
#6208=CLOSED_SHELL('',(#5903,#5904,#5905,#5906,#5907,#5908,#5909,#5910,
#5911,#5912,#5913,#5914,#5915,#5916));
#6829=AXIS2_PLACEMENT_3D('',#9849,#7839,#7840);
#6830=AXIS2_PLACEMENT_3D('',#9850,#7841,#7842);
#6831=AXIS2_PLACEMENT_3D('',#9859,#7847,#7848);
#6832=AXIS2_PLACEMENT_3D('',#9865,#7852,#7853);
#6833=AXIS2_PLACEMENT_3D('',#9872,#7857,#7858);
#6834=AXIS2_PLACEMENT_3D('',#9873,#7859,#7860);
#6835=AXIS2_PLACEMENT_3D('',#9887,#7868,#7869);
#6836=AXIS2_PLACEMENT_3D('',#9891,#7872,#7873);
#6837=AXIS2_PLACEMENT_3D('',#9895,#7876,#7877);
#6838=AXIS2_PLACEMENT_3D('',#9905,#7883,#7884);
#6839=AXIS2_PLACEMENT_3D('',#9907,#7886,#7887);
#6840=AXIS2_PLACEMENT_3D('',#9911,#7889,#7890);
#6841=AXIS2_PLACEMENT_3D('',#9913,#7892,#7893);
#6842=AXIS2_PLACEMENT_3D('',#9915,#7894,#7895);
#6843=AXIS2_PLACEMENT_3D('',#9918,#7897,#7898);
#6844=AXIS2_PLACEMENT_3D('',#9920,#7899,#7900);
#6845=AXIS2_PLACEMENT_3D('',#9921,#7901,#7902);
#6846=AXIS2_PLACEMENT_3D('',#9922,#7903,#7904);
#6847=AXIS2_PLACEMENT_3D('',#9924,#7906,#7907);
#6848=AXIS2_PLACEMENT_3D('',#9926,#7909,#7910);
#6849=AXIS2_PLACEMENT_3D('',#9928,#7912,#7913);
#7839=DIRECTION('axis',(0.,0.,1.));
#7840=DIRECTION('refdir',(1.,0.,0.));
#7841=DIRECTION('center_axis',(0.,0.,1.));
#7842=DIRECTION('ref_axis',(1.,0.,0.));
#7843=DIRECTION('',(1.,0.,0.));
#7844=DIRECTION('',(0.,-1.,0.));
#7845=DIRECTION('',(-1.,0.,0.));
#7846=DIRECTION('',(0.,1.,0.));
#7847=DIRECTION('center_axis',(0.,1.,0.));
#7848=DIRECTION('ref_axis',(-1.,0.,0.));
#7849=DIRECTION('',(0.,0.,1.));
#7850=DIRECTION('',(-1.,0.,0.));
#7851=DIRECTION('',(0.,0.,1.));
#7852=DIRECTION('center_axis',(0.,0.,1.));
#7853=DIRECTION('ref_axis',(1.,0.,0.));
#7854=DIRECTION('',(0.,-1.,0.));
#7855=DIRECTION('',(1.,0.,0.));
#7856=DIRECTION('',(0.,1.,0.));
#7857=DIRECTION('center_axis',(0.,0.,-1.));
#7858=DIRECTION('ref_axis',(1.,0.,0.));
#7859=DIRECTION('center_axis',(-1.,0.,0.));
#7860=DIRECTION('ref_axis',(0.,-1.,0.));
#7861=DIRECTION('',(0.,0.,1.));
#7862=DIRECTION('',(0.,0.707106781186548,0.707106781186548));
#7863=DIRECTION('',(0.,-1.,0.));
#7864=DIRECTION('',(0.,0.707106781186548,-0.707106781186548));
#7865=DIRECTION('',(0.,0.,1.));
#7866=DIRECTION('',(0.,-1.,0.));
#7867=DIRECTION('',(0.,0.,1.));
#7868=DIRECTION('center_axis',(0.,-1.,0.));
#7869=DIRECTION('ref_axis',(1.,0.,0.));
#7870=DIRECTION('',(1.,0.,0.));
#7871=DIRECTION('',(0.,0.,1.));
#7872=DIRECTION('center_axis',(0.,0.,1.));
#7873=DIRECTION('ref_axis',(1.,0.,0.));
#7874=DIRECTION('',(-1.,0.,0.));
#7875=DIRECTION('',(0.,1.,0.));
#7876=DIRECTION('center_axis',(1.,0.,0.));
#7877=DIRECTION('ref_axis',(0.,1.,0.));
#7878=DIRECTION('',(0.,0.,1.));
#7879=DIRECTION('',(0.,-0.707106781186548,0.707106781186548));
#7880=DIRECTION('',(0.,1.,0.));
#7881=DIRECTION('',(0.,-0.707106781186548,-0.707106781186548));
#7882=DIRECTION('',(0.,0.,1.));
#7883=DIRECTION('center_axis',(0.,-1.,0.));
#7884=DIRECTION('ref_axis',(1.,0.,0.));
#7885=DIRECTION('',(-1.,0.,0.));
#7886=DIRECTION('center_axis',(0.,-0.707106781186548,-0.707106781186548));
#7887=DIRECTION('ref_axis',(-1.,0.,0.));
#7888=DIRECTION('',(1.,0.,0.));
#7889=DIRECTION('center_axis',(0.,0.707106781186548,0.707106781186548));
#7890=DIRECTION('ref_axis',(0.,0.707106781186547,-0.707106781186547));
#7891=DIRECTION('',(1.,0.,0.));
#7892=DIRECTION('center_axis',(0.,0.,1.));
#7893=DIRECTION('ref_axis',(1.,0.,0.));
#7894=DIRECTION('center_axis',(0.,0.,-1.));
#7895=DIRECTION('ref_axis',(1.,0.,0.));
#7896=DIRECTION('',(0.,0.,1.));
#7897=DIRECTION('center_axis',(0.,0.,-1.));
#7898=DIRECTION('ref_axis',(1.,0.,0.));
#7899=DIRECTION('center_axis',(0.,-0.707106781186548,0.707106781186548));
#7900=DIRECTION('ref_axis',(0.,0.707106781186547,0.707106781186547));
#7901=DIRECTION('center_axis',(0.,0.,-1.));
#7902=DIRECTION('ref_axis',(1.,0.,0.));
#7903=DIRECTION('center_axis',(0.,0.,1.));
#7904=DIRECTION('ref_axis',(1.,0.,0.));
#7905=DIRECTION('',(-1.,0.,0.));
#7906=DIRECTION('center_axis',(0.,0.,1.));
#7907=DIRECTION('ref_axis',(1.,0.,0.));
#7908=DIRECTION('',(-1.,0.,0.));
#7909=DIRECTION('center_axis',(0.,0.707106781186548,-0.707106781186548));
#7910=DIRECTION('ref_axis',(-1.,0.,0.));
#7911=DIRECTION('',(1.,0.,0.));
#7912=DIRECTION('center_axis',(0.,1.,0.));
#7913=DIRECTION('ref_axis',(-1.,0.,0.));
#9849=CARTESIAN_POINT('',(0.,0.,0.));
#9850=CARTESIAN_POINT('Origin',(0.,0.395,0.25));
#9851=CARTESIAN_POINT('',(-0.5,0.3,0.25));
#9852=CARTESIAN_POINT('',(0.5,0.3,0.25));
#9853=CARTESIAN_POINT('',(0.25,0.3,0.25));
#9854=CARTESIAN_POINT('',(-0.5,0.5,0.25));
#9855=CARTESIAN_POINT('',(-0.5,0.5,0.25));
#9856=CARTESIAN_POINT('',(0.5,0.5,0.25));
#9857=CARTESIAN_POINT('',(0.5,0.5,0.25));
#9858=CARTESIAN_POINT('',(0.5,0.29,0.25));
#9859=CARTESIAN_POINT('Origin',(0.5,0.5,0.25));
#9860=CARTESIAN_POINT('',(-0.5,0.5,0.4));
#9861=CARTESIAN_POINT('',(-0.5,0.5,0.25));
#9862=CARTESIAN_POINT('',(0.5,0.5,0.4));
#9863=CARTESIAN_POINT('',(0.5,0.5,0.4));
#9864=CARTESIAN_POINT('',(0.5,0.5,0.25));
#9865=CARTESIAN_POINT('Origin',(0.,0.,0.4));
#9866=CARTESIAN_POINT('',(-0.5,-0.5,0.4));
#9867=CARTESIAN_POINT('',(-0.5,0.5,0.4));
#9868=CARTESIAN_POINT('',(0.5,-0.5,0.4));
#9869=CARTESIAN_POINT('',(-0.5,-0.5,0.4));
#9870=CARTESIAN_POINT('',(0.5,-0.3,0.4));
#9871=CARTESIAN_POINT('',(-0.2117,2.59257727379495E-17,0.4));
#9872=CARTESIAN_POINT('Origin',(0.,0.,0.4));
#9873=CARTESIAN_POINT('Origin',(-0.5,0.3,0.));
#9874=CARTESIAN_POINT('',(-0.5,0.3,0.15));
#9875=CARTESIAN_POINT('',(-0.5,0.3,0.));
#9876=CARTESIAN_POINT('',(-0.5,0.15,0.));
#9877=CARTESIAN_POINT('',(-0.5,0.225,0.075));
#9878=CARTESIAN_POINT('',(-0.5,-0.15,0.));
#9879=CARTESIAN_POINT('',(-0.5,0.3,0.));
#9880=CARTESIAN_POINT('',(-0.5,-0.3,0.15));
#9881=CARTESIAN_POINT('',(-0.5,-0.075,-0.075));
#9882=CARTESIAN_POINT('',(-0.5,-0.3,0.25));
#9883=CARTESIAN_POINT('',(-0.5,-0.3,0.));
#9884=CARTESIAN_POINT('',(-0.5,-0.5,0.25));
#9885=CARTESIAN_POINT('',(-0.5,-0.29,0.25));
#9886=CARTESIAN_POINT('',(-0.5,-0.5,0.25));
#9887=CARTESIAN_POINT('Origin',(-0.5,-0.5,0.25));
#9888=CARTESIAN_POINT('',(0.5,-0.5,0.25));
#9889=CARTESIAN_POINT('',(-0.5,-0.5,0.25));
#9890=CARTESIAN_POINT('',(0.5,-0.5,0.25));
#9891=CARTESIAN_POINT('Origin',(0.,-0.395,0.25));
#9892=CARTESIAN_POINT('',(0.5,-0.3,0.25));
#9893=CARTESIAN_POINT('',(-0.25,-0.3,0.25));
#9894=CARTESIAN_POINT('',(0.5,-0.5,0.25));
#9895=CARTESIAN_POINT('Origin',(0.5,-0.3,0.));
#9896=CARTESIAN_POINT('',(0.5,-0.3,0.15));
#9897=CARTESIAN_POINT('',(0.5,-0.3,0.));
#9898=CARTESIAN_POINT('',(0.5,-0.15,0.));
#9899=CARTESIAN_POINT('',(0.5,-0.225,0.075));
#9900=CARTESIAN_POINT('',(0.5,0.15,0.));
#9901=CARTESIAN_POINT('',(0.5,-0.3,0.));
#9902=CARTESIAN_POINT('',(0.5,0.3,0.15));
#9903=CARTESIAN_POINT('',(0.5,0.075,-0.075));
#9904=CARTESIAN_POINT('',(0.5,0.3,0.));
#9905=CARTESIAN_POINT('Origin',(-0.5,-0.3,0.));
#9906=CARTESIAN_POINT('',(-0.25,-0.3,0.15));
#9907=CARTESIAN_POINT('Origin',(-0.25,-0.225,0.075));
#9908=CARTESIAN_POINT('',(-0.149388386429468,-0.15,0.));
#9909=CARTESIAN_POINT('',(-0.25,-0.15,0.));
#9910=CARTESIAN_POINT('',(0.149388386429468,-0.15,0.));
#9911=CARTESIAN_POINT('Origin',(0.,0.,-0.15));
#9912=CARTESIAN_POINT('',(-0.25,-0.15,0.));
#9913=CARTESIAN_POINT('Origin',(0.,0.,-0.1));
#9914=CARTESIAN_POINT('',(-0.2117,-2.59257727379495E-17,0.));
#9915=CARTESIAN_POINT('Origin',(0.,0.,0.));
#9916=CARTESIAN_POINT('',(-0.2117,-2.59257727379495E-17,-0.1));
#9917=CARTESIAN_POINT('',(-0.149388386429468,0.15,0.));
#9918=CARTESIAN_POINT('Origin',(0.,0.,0.));
#9919=CARTESIAN_POINT('',(0.149388386429468,0.15,0.));
#9920=CARTESIAN_POINT('Origin',(0.,0.,-0.15));
#9921=CARTESIAN_POINT('Origin',(0.,0.,0.));
#9922=CARTESIAN_POINT('Origin',(0.,0.,0.));
#9923=CARTESIAN_POINT('',(0.25,0.15,0.));
#9924=CARTESIAN_POINT('Origin',(0.,0.,0.));
#9925=CARTESIAN_POINT('',(0.25,0.15,0.));
#9926=CARTESIAN_POINT('Origin',(0.25,0.225,0.075));
#9927=CARTESIAN_POINT('',(0.25,0.3,0.15));
#9928=CARTESIAN_POINT('Origin',(0.5,0.3,0.));
#11655=UNCERTAINTY_MEASURE_WITH_UNIT(LENGTH_MEASURE(0.001),#11749,
'DISTANCE_ACCURACY_VALUE',
'Maximum model space distance between geometric entities at asserted c
onnectivities');
#11699=UNCERTAINTY_MEASURE_WITH_UNIT(LENGTH_MEASURE(0.001),#11749,
'DISTANCE_ACCURACY_VALUE',
'Maximum model space distance between geometric entities at asserted c
onnectivities');
#11704=(
GEOMETRIC_REPRESENTATION_CONTEXT(3)
GLOBAL_UNCERTAINTY_ASSIGNED_CONTEXT((#11655))
GLOBAL_UNIT_ASSIGNED_CONTEXT((#11749,#11751,#11752))
REPRESENTATION_CONTEXT('','3D')
);
#11748=(
GEOMETRIC_REPRESENTATION_CONTEXT(3)
GLOBAL_UNCERTAINTY_ASSIGNED_CONTEXT((#11699))
GLOBAL_UNIT_ASSIGNED_CONTEXT((#11749,#11751,#11752))
REPRESENTATION_CONTEXT('','3D')
);
#11749=(
LENGTH_UNIT()
NAMED_UNIT(*)
SI_UNIT(.CENTI.,.METRE.)
);
#11751=(
NAMED_UNIT(*)
PLANE_ANGLE_UNIT()
SI_UNIT($,.RADIAN.)
);
#11752=(
NAMED_UNIT(*)
SI_UNIT($,.STERADIAN.)
SOLID_ANGLE_UNIT()
);
#11757=SHAPE_DEFINITION_REPRESENTATION(#11805,#11928);
#11805=PRODUCT_DEFINITION_SHAPE('',$,#11977);
#11928=SHAPE_REPRESENTATION('',(#6829),#11704);
#11972=PRODUCT_DEFINITION_CONTEXT('part definition',#12118,'design');
#11977=PRODUCT_DEFINITION('Captive slot nut','Captive slot nut',#12025,
#11972);
#12025=PRODUCT_DEFINITION_FORMATION('',$,#12124);
#12118=APPLICATION_CONTEXT(
'Core Data for Automotive Mechanical Design Process');
#12119=PRODUCT_CONTEXT('part definition',#12118,'mechanical');
#12124=PRODUCT('Captive slot nut','Captive slot nut','Captive slot nut',
(#12119));
#12169=PRESENTATION_STYLE_ASSIGNMENT((#12174));
#12174=SURFACE_STYLE_USAGE(.BOTH.,#12179);
#12179=SURFACE_SIDE_STYLE('',(#12184));
#12184=SURFACE_STYLE_FILL_AREA(#12189);
#12189=FILL_AREA_STYLE('CAD Library Painted - Engineering blue',(#12194));
#12194=FILL_AREA_STYLE_COLOUR('CAD Library Painted - Engineering blue',
#12199);
#12199=COLOUR_RGB('CAD Library Painted - Engineering blue',0.12156862745098,
0.356862745098039,0.6);
ENDSEC;
END-ISO-10303-21;
